ISO-10303-21;
HEADER;
/* Generated by software containing ST-Developer
 * from STEP Tools, Inc. (www.steptools.com) 
 */

FILE_DESCRIPTION(
/* description */ ('Two-link friction support arm'),
/* implementation_level */ '2;1');

FILE_NAME(
/* name */ 'Screen mounting plate (1).step',
/* time_stamp */ '2026-10-27T20:01:49-07:00',
/* author */ (''),
/* organization */ (''),
/* preprocessor_version */ 'ST-DEVELOPER v20.2',
/* originating_system */ 'Autodesk Translation Framework v15.17.0.0',
/* authorisation */ '');

FILE_SCHEMA (('AUTOMOTIVE_DESIGN { 1 0 10303 214 3 1 1 }'));
ENDSEC;

DATA;
#10=MECHANICAL_DESIGN_GEOMETRIC_PRESENTATION_REPRESENTATION('',(#202),#5492);
#180=SHAPE_REPRESENTATION_RELATIONSHIP('SRR','None',#5574,#191);
#191=ADVANCED_BREP_SHAPE_REPRESENTATION('',(#212),#5488);
#202=STYLED_ITEM('',(#5694),#212);
#212=MANIFOLD_SOLID_BREP('Body1',#3179);
#233=FACE_BOUND('',#684,.T.);
#234=FACE_BOUND('',#685,.T.);
#235=FACE_BOUND('',#686,.T.);
#236=FACE_BOUND('',#687,.T.);
#237=FACE_BOUND('',#688,.T.);
#238=FACE_BOUND('',#692,.T.);
#239=FACE_BOUND('',#693,.T.);
#240=FACE_BOUND('',#694,.T.);
#241=FACE_BOUND('',#695,.T.);
#242=FACE_BOUND('',#696,.T.);
#345=PLANE('',#3495);
#346=PLANE('',#3496);
#347=PLANE('',#3497);
#348=PLANE('',#3498);
#349=PLANE('',#3499);
#350=PLANE('',#3500);
#351=PLANE('',#3501);
#352=PLANE('',#3503);
#353=PLANE('',#3506);
#488=FACE_OUTER_BOUND('',#672,.T.);
#489=FACE_OUTER_BOUND('',#673,.T.);
#490=FACE_OUTER_BOUND('',#674,.T.);
#491=FACE_OUTER_BOUND('',#675,.T.);
#492=FACE_OUTER_BOUND('',#676,.T.);
#493=FACE_OUTER_BOUND('',#677,.T.);
#494=FACE_OUTER_BOUND('',#678,.T.);
#495=FACE_OUTER_BOUND('',#679,.T.);
#496=FACE_OUTER_BOUND('',#680,.T.);
#497=FACE_OUTER_BOUND('',#681,.T.);
#498=FACE_OUTER_BOUND('',#682,.T.);
#499=FACE_OUTER_BOUND('',#683,.T.);
#500=FACE_OUTER_BOUND('',#689,.T.);
#501=FACE_OUTER_BOUND('',#690,.T.);
#502=FACE_OUTER_BOUND('',#691,.T.);
#672=EDGE_LOOP('',(#2714,#2715,#2716,#2717));
#673=EDGE_LOOP('',(#2718,#2719,#2720,#2721));
#674=EDGE_LOOP('',(#2722,#2723,#2724,#2725));
#675=EDGE_LOOP('',(#2726,#2727,#2728,#2729));
#676=EDGE_LOOP('',(#2730,#2731,#2732,#2733));
#677=EDGE_LOOP('',(#2734,#2735,#2736,#2737));
#678=EDGE_LOOP('',(#2738,#2739,#2740,#2741));
#679=EDGE_LOOP('',(#2742,#2743,#2744,#2745));
#680=EDGE_LOOP('',(#2746,#2747,#2748,#2749));
#681=EDGE_LOOP('',(#2750,#2751,#2752,#2753));
#682=EDGE_LOOP('',(#2754,#2755,#2756,#2757));
#683=EDGE_LOOP('',(#2758,#2759,#2760,#2761,#2762,#2763,#2764,#2765));
#684=EDGE_LOOP('',(#2766));
#685=EDGE_LOOP('',(#2767));
#686=EDGE_LOOP('',(#2768));
#687=EDGE_LOOP('',(#2769));
#688=EDGE_LOOP('',(#2770));
#689=EDGE_LOOP('',(#2771,#2772,#2773,#2774));
#690=EDGE_LOOP('',(#2775,#2776,#2777,#2778));
#691=EDGE_LOOP('',(#2779,#2780,#2781,#2782,#2783,#2784,#2785,#2786));
#692=EDGE_LOOP('',(#2787));
#693=EDGE_LOOP('',(#2788));
#694=EDGE_LOOP('',(#2789));
#695=EDGE_LOOP('',(#2790));
#696=EDGE_LOOP('',(#2791));
#985=LINE('',#5149,#1298);
#986=LINE('',#5155,#1299);
#987=LINE('',#5161,#1300);
#988=LINE('',#5167,#1301);
#989=LINE('',#5173,#1302);
#990=LINE('',#5178,#1303);
#991=LINE('',#5180,#1304);
#992=LINE('',#5182,#1305);
#993=LINE('',#5183,#1306);
#994=LINE('',#5187,#1307);
#995=LINE('',#5189,#1308);
#996=LINE('',#5191,#1309);
#997=LINE('',#5192,#1310);
#998=LINE('',#5196,#1311);
#999=LINE('',#5197,#1312);
#1000=LINE('',#5198,#1313);
#1001=LINE('',#5201,#1314);
#1002=LINE('',#5203,#1315);
#1003=LINE('',#5204,#1316);
#1004=LINE('',#5206,#1317);
#1005=LINE('',#5207,#1318);
#1006=LINE('',#5210,#1319);
#1007=LINE('',#5212,#1320);
#1008=LINE('',#5213,#1321);
#1009=LINE('',#5216,#1322);
#1010=LINE('',#5220,#1323);
#1011=LINE('',#5221,#1324);
#1298=VECTOR('',#4203,0.329999999999998);
#1299=VECTOR('',#4210,0.329999999999998);
#1300=VECTOR('',#4217,0.329999999999998);
#1301=VECTOR('',#4224,0.329999999999998);
#1302=VECTOR('',#4231,0.425000000000001);
#1303=VECTOR('',#4236,1.);
#1304=VECTOR('',#4237,1.);
#1305=VECTOR('',#4238,1.);
#1306=VECTOR('',#4239,1.);
#1307=VECTOR('',#4242,1.);
#1308=VECTOR('',#4243,1.);
#1309=VECTOR('',#4244,1.);
#1310=VECTOR('',#4245,1.);
#1311=VECTOR('',#4248,1.);
#1312=VECTOR('',#4249,1.);
#1313=VECTOR('',#4250,1.);
#1314=VECTOR('',#4253,1.);
#1315=VECTOR('',#4254,1.);
#1316=VECTOR('',#4255,1.);
#1317=VECTOR('',#4258,1.);
#1318=VECTOR('',#4259,1.);
#1319=VECTOR('',#4262,1.);
#1320=VECTOR('',#4263,1.);
#1321=VECTOR('',#4264,1.);
#1322=VECTOR('',#4267,1.);
#1323=VECTOR('',#4272,1.);
#1324=VECTOR('',#4273,1.);
#1403=CIRCLE('',#3481,0.329999999999998);
#1404=CIRCLE('',#3482,0.329999999999998);
#1405=CIRCLE('',#3484,0.329999999999998);
#1406=CIRCLE('',#3485,0.329999999999998);
#1407=CIRCLE('',#3487,0.329999999999998);
#1408=CIRCLE('',#3488,0.329999999999998);
#1409=CIRCLE('',#3490,0.329999999999998);
#1410=CIRCLE('',#3491,0.329999999999998);
#1411=CIRCLE('',#3493,0.425000000000001);
#1412=CIRCLE('',#3494,0.425000000000001);
#1413=CIRCLE('',#3502,1.5);
#1414=CIRCLE('',#3505,1.5);
#1639=VERTEX_POINT('',#5146);
#1640=VERTEX_POINT('',#5148);
#1641=VERTEX_POINT('',#5152);
#1642=VERTEX_POINT('',#5154);
#1643=VERTEX_POINT('',#5158);
#1644=VERTEX_POINT('',#5160);
#1645=VERTEX_POINT('',#5164);
#1646=VERTEX_POINT('',#5166);
#1647=VERTEX_POINT('',#5170);
#1648=VERTEX_POINT('',#5172);
#1649=VERTEX_POINT('',#5176);
#1650=VERTEX_POINT('',#5177);
#1651=VERTEX_POINT('',#5179);
#1652=VERTEX_POINT('',#5181);
#1653=VERTEX_POINT('',#5185);
#1654=VERTEX_POINT('',#5186);
#1655=VERTEX_POINT('',#5188);
#1656=VERTEX_POINT('',#5190);
#1657=VERTEX_POINT('',#5194);
#1658=VERTEX_POINT('',#5195);
#1659=VERTEX_POINT('',#5200);
#1660=VERTEX_POINT('',#5202);
#1661=VERTEX_POINT('',#5209);
#1662=VERTEX_POINT('',#5211);
#1663=VERTEX_POINT('',#5215);
#1664=VERTEX_POINT('',#5219);
#2011=EDGE_CURVE('',#1639,#1639,#1403,.T.);
#2012=EDGE_CURVE('',#1639,#1640,#985,.T.);
#2013=EDGE_CURVE('',#1640,#1640,#1404,.T.);
#2014=EDGE_CURVE('',#1641,#1641,#1405,.T.);
#2015=EDGE_CURVE('',#1641,#1642,#986,.T.);
#2016=EDGE_CURVE('',#1642,#1642,#1406,.T.);
#2017=EDGE_CURVE('',#1643,#1643,#1407,.T.);
#2018=EDGE_CURVE('',#1643,#1644,#987,.T.);
#2019=EDGE_CURVE('',#1644,#1644,#1408,.T.);
#2020=EDGE_CURVE('',#1645,#1645,#1409,.T.);
#2021=EDGE_CURVE('',#1645,#1646,#988,.T.);
#2022=EDGE_CURVE('',#1646,#1646,#1410,.T.);
#2023=EDGE_CURVE('',#1647,#1647,#1411,.T.);
#2024=EDGE_CURVE('',#1647,#1648,#989,.T.);
#2025=EDGE_CURVE('',#1648,#1648,#1412,.T.);
#2026=EDGE_CURVE('',#1649,#1650,#990,.T.);
#2027=EDGE_CURVE('',#1651,#1649,#991,.T.);
#2028=EDGE_CURVE('',#1652,#1651,#992,.T.);
#2029=EDGE_CURVE('',#1650,#1652,#993,.T.);
#2030=EDGE_CURVE('',#1653,#1654,#994,.T.);
#2031=EDGE_CURVE('',#1653,#1655,#995,.T.);
#2032=EDGE_CURVE('',#1656,#1655,#996,.T.);
#2033=EDGE_CURVE('',#1654,#1656,#997,.T.);
#2034=EDGE_CURVE('',#1657,#1658,#998,.T.);
#2035=EDGE_CURVE('',#1654,#1657,#999,.T.);
#2036=EDGE_CURVE('',#1658,#1656,#1000,.T.);
#2037=EDGE_CURVE('',#1652,#1659,#1001,.T.);
#2038=EDGE_CURVE('',#1660,#1651,#1002,.T.);
#2039=EDGE_CURVE('',#1659,#1660,#1003,.T.);
#2040=EDGE_CURVE('',#1659,#1653,#1004,.T.);
#2041=EDGE_CURVE('',#1655,#1660,#1005,.T.);
#2042=EDGE_CURVE('',#1661,#1658,#1006,.T.);
#2043=EDGE_CURVE('',#1662,#1661,#1007,.T.);
#2044=EDGE_CURVE('',#1657,#1662,#1008,.T.);
#2045=EDGE_CURVE('',#1649,#1663,#1009,.T.);
#2046=EDGE_CURVE('',#1663,#1661,#1413,.T.);
#2047=EDGE_CURVE('',#1664,#1650,#1010,.T.);
#2048=EDGE_CURVE('',#1663,#1664,#1011,.T.);
#2049=EDGE_CURVE('',#1664,#1662,#1414,.T.);
#2714=ORIENTED_EDGE('',*,*,#2011,.F.);
#2715=ORIENTED_EDGE('',*,*,#2012,.T.);
#2716=ORIENTED_EDGE('',*,*,#2013,.F.);
#2717=ORIENTED_EDGE('',*,*,#2012,.F.);
#2718=ORIENTED_EDGE('',*,*,#2014,.F.);
#2719=ORIENTED_EDGE('',*,*,#2015,.T.);
#2720=ORIENTED_EDGE('',*,*,#2016,.F.);
#2721=ORIENTED_EDGE('',*,*,#2015,.F.);
#2722=ORIENTED_EDGE('',*,*,#2017,.F.);
#2723=ORIENTED_EDGE('',*,*,#2018,.T.);
#2724=ORIENTED_EDGE('',*,*,#2019,.F.);
#2725=ORIENTED_EDGE('',*,*,#2018,.F.);
#2726=ORIENTED_EDGE('',*,*,#2020,.F.);
#2727=ORIENTED_EDGE('',*,*,#2021,.T.);
#2728=ORIENTED_EDGE('',*,*,#2022,.F.);
#2729=ORIENTED_EDGE('',*,*,#2021,.F.);
#2730=ORIENTED_EDGE('',*,*,#2023,.F.);
#2731=ORIENTED_EDGE('',*,*,#2024,.T.);
#2732=ORIENTED_EDGE('',*,*,#2025,.F.);
#2733=ORIENTED_EDGE('',*,*,#2024,.F.);
#2734=ORIENTED_EDGE('',*,*,#2026,.F.);
#2735=ORIENTED_EDGE('',*,*,#2027,.F.);
#2736=ORIENTED_EDGE('',*,*,#2028,.F.);
#2737=ORIENTED_EDGE('',*,*,#2029,.F.);
#2738=ORIENTED_EDGE('',*,*,#2030,.F.);
#2739=ORIENTED_EDGE('',*,*,#2031,.T.);
#2740=ORIENTED_EDGE('',*,*,#2032,.F.);
#2741=ORIENTED_EDGE('',*,*,#2033,.F.);
#2742=ORIENTED_EDGE('',*,*,#2034,.F.);
#2743=ORIENTED_EDGE('',*,*,#2035,.F.);
#2744=ORIENTED_EDGE('',*,*,#2033,.T.);
#2745=ORIENTED_EDGE('',*,*,#2036,.F.);
#2746=ORIENTED_EDGE('',*,*,#2037,.F.);
#2747=ORIENTED_EDGE('',*,*,#2028,.T.);
#2748=ORIENTED_EDGE('',*,*,#2038,.F.);
#2749=ORIENTED_EDGE('',*,*,#2039,.F.);
#2750=ORIENTED_EDGE('',*,*,#2040,.F.);
#2751=ORIENTED_EDGE('',*,*,#2039,.T.);
#2752=ORIENTED_EDGE('',*,*,#2041,.F.);
#2753=ORIENTED_EDGE('',*,*,#2031,.F.);
#2754=ORIENTED_EDGE('',*,*,#2034,.T.);
#2755=ORIENTED_EDGE('',*,*,#2042,.F.);
#2756=ORIENTED_EDGE('',*,*,#2043,.F.);
#2757=ORIENTED_EDGE('',*,*,#2044,.F.);
#2758=ORIENTED_EDGE('',*,*,#2036,.T.);
#2759=ORIENTED_EDGE('',*,*,#2032,.T.);
#2760=ORIENTED_EDGE('',*,*,#2041,.T.);
#2761=ORIENTED_EDGE('',*,*,#2038,.T.);
#2762=ORIENTED_EDGE('',*,*,#2027,.T.);
#2763=ORIENTED_EDGE('',*,*,#2045,.T.);
#2764=ORIENTED_EDGE('',*,*,#2046,.T.);
#2765=ORIENTED_EDGE('',*,*,#2042,.T.);
#2766=ORIENTED_EDGE('',*,*,#2025,.T.);
#2767=ORIENTED_EDGE('',*,*,#2022,.T.);
#2768=ORIENTED_EDGE('',*,*,#2019,.T.);
#2769=ORIENTED_EDGE('',*,*,#2016,.T.);
#2770=ORIENTED_EDGE('',*,*,#2013,.T.);
#2771=ORIENTED_EDGE('',*,*,#2026,.T.);
#2772=ORIENTED_EDGE('',*,*,#2047,.F.);
#2773=ORIENTED_EDGE('',*,*,#2048,.F.);
#2774=ORIENTED_EDGE('',*,*,#2045,.F.);
#2775=ORIENTED_EDGE('',*,*,#2043,.T.);
#2776=ORIENTED_EDGE('',*,*,#2046,.F.);
#2777=ORIENTED_EDGE('',*,*,#2048,.T.);
#2778=ORIENTED_EDGE('',*,*,#2049,.T.);
#2779=ORIENTED_EDGE('',*,*,#2044,.T.);
#2780=ORIENTED_EDGE('',*,*,#2049,.F.);
#2781=ORIENTED_EDGE('',*,*,#2047,.T.);
#2782=ORIENTED_EDGE('',*,*,#2029,.T.);
#2783=ORIENTED_EDGE('',*,*,#2037,.T.);
#2784=ORIENTED_EDGE('',*,*,#2040,.T.);
#2785=ORIENTED_EDGE('',*,*,#2030,.T.);
#2786=ORIENTED_EDGE('',*,*,#2035,.T.);
#2787=ORIENTED_EDGE('',*,*,#2023,.T.);
#2788=ORIENTED_EDGE('',*,*,#2020,.T.);
#2789=ORIENTED_EDGE('',*,*,#2017,.T.);
#2790=ORIENTED_EDGE('',*,*,#2014,.T.);
#2791=ORIENTED_EDGE('',*,*,#2011,.T.);
#2982=CYLINDRICAL_SURFACE('',#3480,0.329999999999998);
#2983=CYLINDRICAL_SURFACE('',#3483,0.329999999999998);
#2984=CYLINDRICAL_SURFACE('',#3486,0.329999999999998);
#2985=CYLINDRICAL_SURFACE('',#3489,0.329999999999998);
#2986=CYLINDRICAL_SURFACE('',#3492,0.425000000000001);
#2987=CYLINDRICAL_SURFACE('',#3504,1.5);
#3119=ADVANCED_FACE('',(#488),#2982,.F.);
#3120=ADVANCED_FACE('',(#489),#2983,.F.);
#3121=ADVANCED_FACE('',(#490),#2984,.F.);
#3122=ADVANCED_FACE('',(#491),#2985,.F.);
#3123=ADVANCED_FACE('',(#492),#2986,.F.);
#3124=ADVANCED_FACE('',(#493),#345,.T.);
#3125=ADVANCED_FACE('',(#494),#346,.T.);
#3126=ADVANCED_FACE('',(#495),#347,.T.);
#3127=ADVANCED_FACE('',(#496),#348,.T.);
#3128=ADVANCED_FACE('',(#497),#349,.T.);
#3129=ADVANCED_FACE('',(#498),#350,.T.);
#3130=ADVANCED_FACE('',(#499,#233,#234,#235,#236,#237),#351,.T.);
#3131=ADVANCED_FACE('',(#500),#352,.T.);
#3132=ADVANCED_FACE('',(#501),#2987,.T.);
#3133=ADVANCED_FACE('',(#502,#238,#239,#240,#241,#242),#353,.F.);
#3179=CLOSED_SHELL('',(#3119,#3120,#3121,#3122,#3123,#3124,#3125,#3126,
#3127,#3128,#3129,#3130,#3131,#3132,#3133));
#3479=AXIS2_PLACEMENT_3D('',#5144,#4197,#4198);
#3480=AXIS2_PLACEMENT_3D('',#5145,#4199,#4200);
#3481=AXIS2_PLACEMENT_3D('',#5147,#4201,#4202);
#3482=AXIS2_PLACEMENT_3D('',#5150,#4204,#4205);
#3483=AXIS2_PLACEMENT_3D('',#5151,#4206,#4207);
#3484=AXIS2_PLACEMENT_3D('',#5153,#4208,#4209);
#3485=AXIS2_PLACEMENT_3D('',#5156,#4211,#4212);
#3486=AXIS2_PLACEMENT_3D('',#5157,#4213,#4214);
#3487=AXIS2_PLACEMENT_3D('',#5159,#4215,#4216);
#3488=AXIS2_PLACEMENT_3D('',#5162,#4218,#4219);
#3489=AXIS2_PLACEMENT_3D('',#5163,#4220,#4221);
#3490=AXIS2_PLACEMENT_3D('',#5165,#4222,#4223);
#3491=AXIS2_PLACEMENT_3D('',#5168,#4225,#4226);
#3492=AXIS2_PLACEMENT_3D('',#5169,#4227,#4228);
#3493=AXIS2_PLACEMENT_3D('',#5171,#4229,#4230);
#3494=AXIS2_PLACEMENT_3D('',#5174,#4232,#4233);
#3495=AXIS2_PLACEMENT_3D('',#5175,#4234,#4235);
#3496=AXIS2_PLACEMENT_3D('',#5184,#4240,#4241);
#3497=AXIS2_PLACEMENT_3D('',#5193,#4246,#4247);
#3498=AXIS2_PLACEMENT_3D('',#5199,#4251,#4252);
#3499=AXIS2_PLACEMENT_3D('',#5205,#4256,#4257);
#3500=AXIS2_PLACEMENT_3D('',#5208,#4260,#4261);
#3501=AXIS2_PLACEMENT_3D('',#5214,#4265,#4266);
#3502=AXIS2_PLACEMENT_3D('',#5217,#4268,#4269);
#3503=AXIS2_PLACEMENT_3D('',#5218,#4270,#4271);
#3504=AXIS2_PLACEMENT_3D('',#5222,#4274,#4275);
#3505=AXIS2_PLACEMENT_3D('',#5223,#4276,#4277);
#3506=AXIS2_PLACEMENT_3D('',#5224,#4278,#4279);
#4197=DIRECTION('axis',(0.,0.,1.));
#4198=DIRECTION('refdir',(1.,0.,0.));
#4199=DIRECTION('center_axis',(0.,1.,0.));
#4200=DIRECTION('ref_axis',(1.,0.,0.));
#4201=DIRECTION('center_axis',(0.,1.,0.));
#4202=DIRECTION('ref_axis',(1.,0.,0.));
#4203=DIRECTION('',(0.,1.,0.));
#4204=DIRECTION('center_axis',(0.,-1.,0.));
#4205=DIRECTION('ref_axis',(1.,0.,0.));
#4206=DIRECTION('center_axis',(0.,1.,0.));
#4207=DIRECTION('ref_axis',(1.,0.,0.));
#4208=DIRECTION('center_axis',(0.,1.,0.));
#4209=DIRECTION('ref_axis',(1.,0.,0.));
#4210=DIRECTION('',(0.,1.,0.));
#4211=DIRECTION('center_axis',(0.,-1.,0.));
#4212=DIRECTION('ref_axis',(1.,0.,0.));
#4213=DIRECTION('center_axis',(0.,1.,0.));
#4214=DIRECTION('ref_axis',(1.,0.,0.));
#4215=DIRECTION('center_axis',(0.,1.,0.));
#4216=DIRECTION('ref_axis',(1.,0.,0.));
#4217=DIRECTION('',(0.,1.,0.));
#4218=DIRECTION('center_axis',(0.,-1.,0.));
#4219=DIRECTION('ref_axis',(1.,0.,0.));
#4220=DIRECTION('center_axis',(0.,1.,0.));
#4221=DIRECTION('ref_axis',(1.,0.,0.));
#4222=DIRECTION('center_axis',(0.,1.,0.));
#4223=DIRECTION('ref_axis',(1.,0.,0.));
#4224=DIRECTION('',(0.,1.,0.));
#4225=DIRECTION('center_axis',(0.,-1.,0.));
#4226=DIRECTION('ref_axis',(1.,0.,0.));
#4227=DIRECTION('center_axis',(0.,1.,0.));
#4228=DIRECTION('ref_axis',(1.,0.,0.));
#4229=DIRECTION('center_axis',(0.,1.,0.));
#4230=DIRECTION('ref_axis',(1.,0.,0.));
#4231=DIRECTION('',(0.,1.,0.));
#4232=DIRECTION('center_axis',(0.,-1.,0.));
#4233=DIRECTION('ref_axis',(1.,0.,0.));
#4234=DIRECTION('center_axis',(0.,0.,-1.));
#4235=DIRECTION('ref_axis',(-1.,0.,0.));
#4236=DIRECTION('',(0.,-1.,0.));
#4237=DIRECTION('',(-1.,0.,0.));
#4238=DIRECTION('',(0.,1.,0.));
#4239=DIRECTION('',(1.,0.,0.));
#4240=DIRECTION('center_axis',(-1.,0.,0.));
#4241=DIRECTION('ref_axis',(0.,0.,1.));
#4242=DIRECTION('',(0.,0.,-1.));
#4243=DIRECTION('',(0.,1.,0.));
#4244=DIRECTION('',(0.,0.,1.));
#4245=DIRECTION('',(0.,1.,0.));
#4246=DIRECTION('center_axis',(0.,0.,-1.));
#4247=DIRECTION('ref_axis',(-1.,0.,0.));
#4248=DIRECTION('',(0.,1.,0.));
#4249=DIRECTION('',(1.,0.,0.));
#4250=DIRECTION('',(-1.,0.,0.));
#4251=DIRECTION('center_axis',(1.,0.,0.));
#4252=DIRECTION('ref_axis',(0.,0.,-1.));
#4253=DIRECTION('',(0.,0.,1.));
#4254=DIRECTION('',(0.,0.,-1.));
#4255=DIRECTION('',(0.,1.,0.));
#4256=DIRECTION('center_axis',(0.,0.,1.));
#4257=DIRECTION('ref_axis',(1.,0.,0.));
#4258=DIRECTION('',(-1.,0.,0.));
#4259=DIRECTION('',(1.,0.,0.));
#4260=DIRECTION('center_axis',(-1.,0.,0.));
#4261=DIRECTION('ref_axis',(0.,0.,1.));
#4262=DIRECTION('',(0.,0.,1.));
#4263=DIRECTION('',(0.,1.,0.));
#4264=DIRECTION('',(0.,0.,-1.));
#4265=DIRECTION('center_axis',(0.,1.,0.));
#4266=DIRECTION('ref_axis',(1.,0.,0.));
#4267=DIRECTION('',(0.,0.,-1.));
#4268=DIRECTION('center_axis',(0.,1.,0.));
#4269=DIRECTION('ref_axis',(1.,0.,0.));
#4270=DIRECTION('center_axis',(1.,0.,0.));
#4271=DIRECTION('ref_axis',(0.,0.,-1.));
#4272=DIRECTION('',(0.,0.,1.));
#4273=DIRECTION('',(0.,-1.,0.));
#4274=DIRECTION('center_axis',(0.,1.,0.));
#4275=DIRECTION('ref_axis',(-1.83697019872103E-16,0.,-1.));
#4276=DIRECTION('center_axis',(0.,1.,0.));
#4277=DIRECTION('ref_axis',(1.,0.,0.));
#4278=DIRECTION('center_axis',(0.,1.,0.));
#4279=DIRECTION('ref_axis',(1.,0.,0.));
#5144=CARTESIAN_POINT('',(0.,0.,0.));
#5145=CARTESIAN_POINT('Origin',(28.75,1.98,12.25));
#5146=CARTESIAN_POINT('',(28.42,2.08,12.25));
#5147=CARTESIAN_POINT('Origin',(28.75,2.08,12.25));
#5148=CARTESIAN_POINT('',(28.42,2.88,12.25));
#5149=CARTESIAN_POINT('',(28.42,1.98,12.25));
#5150=CARTESIAN_POINT('Origin',(28.75,2.88,12.25));
#5151=CARTESIAN_POINT('Origin',(21.25,1.98,19.75));
#5152=CARTESIAN_POINT('',(20.92,2.08,19.75));
#5153=CARTESIAN_POINT('Origin',(21.25,2.08,19.75));
#5154=CARTESIAN_POINT('',(20.92,2.88,19.75));
#5155=CARTESIAN_POINT('',(20.92,1.98,19.75));
#5156=CARTESIAN_POINT('Origin',(21.25,2.88,19.75));
#5157=CARTESIAN_POINT('Origin',(21.25,1.98,12.25));
#5158=CARTESIAN_POINT('',(20.92,2.08,12.25));
#5159=CARTESIAN_POINT('Origin',(21.25,2.08,12.25));
#5160=CARTESIAN_POINT('',(20.92,2.88,12.25));
#5161=CARTESIAN_POINT('',(20.92,1.98,12.25));
#5162=CARTESIAN_POINT('Origin',(21.25,2.88,12.25));
#5163=CARTESIAN_POINT('Origin',(28.75,1.98,19.75));
#5164=CARTESIAN_POINT('',(28.42,2.08,19.75));
#5165=CARTESIAN_POINT('Origin',(28.75,2.08,19.75));
#5166=CARTESIAN_POINT('',(28.42,2.88,19.75));
#5167=CARTESIAN_POINT('',(28.42,1.98,19.75));
#5168=CARTESIAN_POINT('Origin',(28.75,2.88,19.75));
#5169=CARTESIAN_POINT('Origin',(25.,1.98,8.));
#5170=CARTESIAN_POINT('',(24.575,2.08,8.));
#5171=CARTESIAN_POINT('Origin',(25.,2.08,8.));
#5172=CARTESIAN_POINT('',(24.575,2.88,8.));
#5173=CARTESIAN_POINT('',(24.575,1.98,8.));
#5174=CARTESIAN_POINT('Origin',(25.,2.88,8.));
#5175=CARTESIAN_POINT('Origin',(30.,2.08,11.));
#5176=CARTESIAN_POINT('',(26.,2.88,11.));
#5177=CARTESIAN_POINT('',(26.,2.08,11.));
#5178=CARTESIAN_POINT('',(26.,2.08,11.));
#5179=CARTESIAN_POINT('',(30.,2.88,11.));
#5180=CARTESIAN_POINT('',(20.,2.88,11.));
#5181=CARTESIAN_POINT('',(30.,2.08,11.));
#5182=CARTESIAN_POINT('',(30.,2.08,11.));
#5183=CARTESIAN_POINT('',(20.,2.08,11.));
#5184=CARTESIAN_POINT('Origin',(20.,2.08,11.));
#5185=CARTESIAN_POINT('',(20.,2.08,21.));
#5186=CARTESIAN_POINT('',(20.,2.08,11.));
#5187=CARTESIAN_POINT('',(20.,2.08,21.));
#5188=CARTESIAN_POINT('',(20.,2.88,21.));
#5189=CARTESIAN_POINT('',(20.,2.08,21.));
#5190=CARTESIAN_POINT('',(20.,2.88,11.));
#5191=CARTESIAN_POINT('',(20.,2.88,21.));
#5192=CARTESIAN_POINT('',(20.,2.08,11.));
#5193=CARTESIAN_POINT('Origin',(30.,2.08,11.));
#5194=CARTESIAN_POINT('',(24.,2.08,11.));
#5195=CARTESIAN_POINT('',(24.,2.88,11.));
#5196=CARTESIAN_POINT('',(24.,2.08,11.));
#5197=CARTESIAN_POINT('',(20.,2.08,11.));
#5198=CARTESIAN_POINT('',(20.,2.88,11.));
#5199=CARTESIAN_POINT('Origin',(30.,2.08,21.));
#5200=CARTESIAN_POINT('',(30.,2.08,21.));
#5201=CARTESIAN_POINT('',(30.,2.08,11.));
#5202=CARTESIAN_POINT('',(30.,2.88,21.));
#5203=CARTESIAN_POINT('',(30.,2.88,11.));
#5204=CARTESIAN_POINT('',(30.,2.08,21.));
#5205=CARTESIAN_POINT('Origin',(20.,2.08,21.));
#5206=CARTESIAN_POINT('',(30.,2.08,21.));
#5207=CARTESIAN_POINT('',(30.,2.88,21.));
#5208=CARTESIAN_POINT('Origin',(24.,2.08,8.));
#5209=CARTESIAN_POINT('',(24.,2.88,9.11803398874989));
#5210=CARTESIAN_POINT('',(24.,2.88,12.));
#5211=CARTESIAN_POINT('',(24.,2.08,9.11803398874989));
#5212=CARTESIAN_POINT('',(24.,2.08,9.11803398874989));
#5213=CARTESIAN_POINT('',(24.,2.08,12.));
#5214=CARTESIAN_POINT('Origin',(25.,2.88,8.));
#5215=CARTESIAN_POINT('',(26.,2.88,9.11803398874989));
#5216=CARTESIAN_POINT('',(26.,2.88,8.));
#5217=CARTESIAN_POINT('Origin',(25.,2.88,8.));
#5218=CARTESIAN_POINT('Origin',(26.,2.08,12.));
#5219=CARTESIAN_POINT('',(26.,2.08,9.11803398874989));
#5220=CARTESIAN_POINT('',(26.,2.08,8.));
#5221=CARTESIAN_POINT('',(26.,2.08,9.11803398874989));
#5222=CARTESIAN_POINT('Origin',(25.,2.08,8.));
#5223=CARTESIAN_POINT('Origin',(25.,2.08,8.));
#5224=CARTESIAN_POINT('Origin',(25.,2.08,8.));
#5471=UNCERTAINTY_MEASURE_WITH_UNIT(LENGTH_MEASURE(0.001),#5493,
'DISTANCE_ACCURACY_VALUE',
'Maximum model space distance between geometric entities at asserted c
onnectivities');
#5475=UNCERTAINTY_MEASURE_WITH_UNIT(LENGTH_MEASURE(0.001),#5493,
'DISTANCE_ACCURACY_VALUE',
'Maximum model space distance between geometric entities at asserted c
onnectivities');
#5488=(
GEOMETRIC_REPRESENTATION_CONTEXT(3)
GLOBAL_UNCERTAINTY_ASSIGNED_CONTEXT((#5471))
GLOBAL_UNIT_ASSIGNED_CONTEXT((#5493,#5495,#5496))
REPRESENTATION_CONTEXT('','3D')
);
#5492=(
GEOMETRIC_REPRESENTATION_CONTEXT(3)
GLOBAL_UNCERTAINTY_ASSIGNED_CONTEXT((#5475))
GLOBAL_UNIT_ASSIGNED_CONTEXT((#5493,#5495,#5496))
REPRESENTATION_CONTEXT('','3D')
);
#5493=(
LENGTH_UNIT()
NAMED_UNIT(*)
SI_UNIT(.CENTI.,.METRE.)
);
#5495=(
NAMED_UNIT(*)
PLANE_ANGLE_UNIT()
SI_UNIT($,.RADIAN.)
);
#5496=(
NAMED_UNIT(*)
SI_UNIT($,.STERADIAN.)
SOLID_ANGLE_UNIT()
);
#5509=SHAPE_DEFINITION_REPRESENTATION(#5534,#5574);
#5534=PRODUCT_DEFINITION_SHAPE('',$,#5591);
#5574=SHAPE_REPRESENTATION('',(#3479),#5488);
#5578=PRODUCT_DEFINITION_CONTEXT('part definition',#5628,'design');
#5591=PRODUCT_DEFINITION('Screen mounting plate (1)',
'Screen mounting plate (1)',#5607,#5578);
#5607=PRODUCT_DEFINITION_FORMATION('',$,#5642);
#5628=APPLICATION_CONTEXT(
'Core Data for Automotive Mechanical Design Process');
#5629=PRODUCT_CONTEXT('part definition',#5628,'mechanical');
#5642=PRODUCT('Screen mounting plate (1)','Screen mounting plate (1)',
'Screen mounting plate (1)',(#5629));
#5688=COLOUR_RGB('Sky Blue',0.24,0.69,0.87);
#5689=FILL_AREA_STYLE_COLOUR('',#5688);
#5690=FILL_AREA_STYLE('',(#5689));
#5691=SURFACE_STYLE_FILL_AREA(#5690);
#5692=SURFACE_SIDE_STYLE('',(#5691));
#5693=SURFACE_STYLE_USAGE(.BOTH.,#5692);
#5694=PRESENTATION_STYLE_ASSIGNMENT((#5693));
ENDSEC;
END-ISO-10303-21;
